ISO-10303-21;
HEADER;
/* Generated by software containing ST-Developer
 * from STEP Tools, Inc. (www.steptools.com) 
 */

FILE_DESCRIPTION(
/* description */ ('Manual piston pump'),
/* implementation_level */ '2;1');

FILE_NAME(
/* name */ 'Hex Nut - M5.step',
/* time_stamp */ '2026-11-02T16:54:23-08:00',
/* author */ (''),
/* organization */ (''),
/* preprocessor_version */ 'ST-DEVELOPER v20.2',
/* originating_system */ 'Autodesk Translation Framework v15.17.0.0',
/* authorisation */ '');

FILE_SCHEMA (('AUTOMOTIVE_DESIGN { 1 0 10303 214 3 1 1 }'));
ENDSEC;

DATA;
#10=MECHANICAL_DESIGN_GEOMETRIC_PRESENTATION_REPRESENTATION('',(#703),#19043);
#510=(
BOUNDED_CURVE()
B_SPLINE_CURVE(2,(#15259,#15260,#15261),.UNSPECIFIED.,.F.,.F.)
B_SPLINE_CURVE_WITH_KNOTS((3,3),(0.140651836354967,0.670383167684795),
 .UNSPECIFIED.)
CURVE()
GEOMETRIC_REPRESENTATION_ITEM()
RATIONAL_B_SPLINE_CURVE((1.11602540378444,1.28867513459481,1.11602540378444))
REPRESENTATION_ITEM('')
);
#511=(
BOUNDED_CURVE()
B_SPLINE_CURVE(2,(#15263,#15264,#15265),.UNSPECIFIED.,.F.,.F.)
B_SPLINE_CURVE_WITH_KNOTS((3,3),(0.140651836354967,0.670383167684795),
 .UNSPECIFIED.)
CURVE()
GEOMETRIC_REPRESENTATION_ITEM()
RATIONAL_B_SPLINE_CURVE((1.11602540378444,1.28867513459481,1.11602540378444))
REPRESENTATION_ITEM('')
);
#512=(
BOUNDED_CURVE()
B_SPLINE_CURVE(2,(#15270,#15271,#15272),.UNSPECIFIED.,.F.,.F.)
B_SPLINE_CURVE_WITH_KNOTS((3,3),(0.140651836354967,0.670383167684795),
 .UNSPECIFIED.)
CURVE()
GEOMETRIC_REPRESENTATION_ITEM()
RATIONAL_B_SPLINE_CURVE((1.11602540378444,1.28867513459481,1.11602540378444))
REPRESENTATION_ITEM('')
);
#513=(
BOUNDED_CURVE()
B_SPLINE_CURVE(2,(#15274,#15275,#15276),.UNSPECIFIED.,.F.,.F.)
B_SPLINE_CURVE_WITH_KNOTS((3,3),(0.140651836354967,0.670383167684795),
 .UNSPECIFIED.)
CURVE()
GEOMETRIC_REPRESENTATION_ITEM()
RATIONAL_B_SPLINE_CURVE((1.11602540378444,1.28867513459481,1.11602540378444))
REPRESENTATION_ITEM('')
);
#514=(
BOUNDED_CURVE()
B_SPLINE_CURVE(2,(#15278,#15279,#15280),.UNSPECIFIED.,.F.,.F.)
B_SPLINE_CURVE_WITH_KNOTS((3,3),(0.140651836354967,0.670383167684795),
 .UNSPECIFIED.)
CURVE()
GEOMETRIC_REPRESENTATION_ITEM()
RATIONAL_B_SPLINE_CURVE((1.11602540378444,1.28867513459481,1.11602540378444))
REPRESENTATION_ITEM('')
);
#515=(
BOUNDED_CURVE()
B_SPLINE_CURVE(2,(#15281,#15282,#15283),.UNSPECIFIED.,.F.,.F.)
B_SPLINE_CURVE_WITH_KNOTS((3,3),(0.140651836354967,0.670383167684795),
 .UNSPECIFIED.)
CURVE()
GEOMETRIC_REPRESENTATION_ITEM()
RATIONAL_B_SPLINE_CURVE((1.11602540378444,1.28867513459481,1.11602540378444))
REPRESENTATION_ITEM('')
);
#516=(
BOUNDED_CURVE()
B_SPLINE_CURVE(2,(#15290,#15291,#15292),.UNSPECIFIED.,.F.,.F.)
B_SPLINE_CURVE_WITH_KNOTS((3,3),(0.140651836354967,0.670383167684795),
 .UNSPECIFIED.)
CURVE()
GEOMETRIC_REPRESENTATION_ITEM()
RATIONAL_B_SPLINE_CURVE((1.11602540378444,1.28867513459481,1.11602540378444))
REPRESENTATION_ITEM('')
);
#517=(
BOUNDED_CURVE()
B_SPLINE_CURVE(2,(#15294,#15295,#15296),.UNSPECIFIED.,.F.,.F.)
B_SPLINE_CURVE_WITH_KNOTS((3,3),(0.140651836354967,0.670383167684796),
 .UNSPECIFIED.)
CURVE()
GEOMETRIC_REPRESENTATION_ITEM()
RATIONAL_B_SPLINE_CURVE((1.11602540378444,1.28867513459481,1.11602540378444))
REPRESENTATION_ITEM('')
);
#518=(
BOUNDED_CURVE()
B_SPLINE_CURVE(2,(#15298,#15299,#15300),.UNSPECIFIED.,.F.,.F.)
B_SPLINE_CURVE_WITH_KNOTS((3,3),(0.140651836354967,0.670383167684795),
 .UNSPECIFIED.)
CURVE()
GEOMETRIC_REPRESENTATION_ITEM()
RATIONAL_B_SPLINE_CURVE((1.11602540378444,1.28867513459481,1.11602540378444))
REPRESENTATION_ITEM('')
);
#519=(
BOUNDED_CURVE()
B_SPLINE_CURVE(2,(#15302,#15303,#15304),.UNSPECIFIED.,.F.,.F.)
B_SPLINE_CURVE_WITH_KNOTS((3,3),(0.140651836354967,0.670383167684795),
 .UNSPECIFIED.)
CURVE()
GEOMETRIC_REPRESENTATION_ITEM()
RATIONAL_B_SPLINE_CURVE((1.11602540378444,1.28867513459482,1.11602540378444))
REPRESENTATION_ITEM('')
);
#520=(
BOUNDED_CURVE()
B_SPLINE_CURVE(2,(#15306,#15307,#15308),.UNSPECIFIED.,.F.,.F.)
B_SPLINE_CURVE_WITH_KNOTS((3,3),(0.140651836354967,0.670383167684795),
 .UNSPECIFIED.)
CURVE()
GEOMETRIC_REPRESENTATION_ITEM()
RATIONAL_B_SPLINE_CURVE((1.11602540378444,1.28867513459481,1.11602540378444))
REPRESENTATION_ITEM('')
);
#521=(
BOUNDED_CURVE()
B_SPLINE_CURVE(2,(#15309,#15310,#15311),.UNSPECIFIED.,.F.,.F.)
B_SPLINE_CURVE_WITH_KNOTS((3,3),(0.140651836354967,0.670383167684795),
 .UNSPECIFIED.)
CURVE()
GEOMETRIC_REPRESENTATION_ITEM()
RATIONAL_B_SPLINE_CURVE((1.11602540378444,1.28867513459481,1.11602540378444))
REPRESENTATION_ITEM('')
);
#532=CONICAL_SURFACE('',#10515,0.47094010767585,1.0471975511966);
#533=CONICAL_SURFACE('',#10517,0.47094010767585,1.0471975511966);
#577=SHAPE_REPRESENTATION_RELATIONSHIP('SRR','None',#19323,#640);
#640=ADVANCED_BREP_SHAPE_REPRESENTATION('',(#774),#18990);
#703=STYLED_ITEM('',(#19663),#774);
#774=MANIFOLD_SOLID_BREP('Body1',#9488);
#887=FACE_BOUND('',#2072,.T.);
#888=FACE_BOUND('',#2074,.T.);
#1146=CYLINDRICAL_SURFACE('',#10522,0.2117);
#1427=FACE_OUTER_BOUND('',#2062,.T.);
#1428=FACE_OUTER_BOUND('',#2063,.T.);
#1429=FACE_OUTER_BOUND('',#2064,.T.);
#1430=FACE_OUTER_BOUND('',#2065,.T.);
#1431=FACE_OUTER_BOUND('',#2066,.T.);
#1432=FACE_OUTER_BOUND('',#2067,.T.);
#1433=FACE_OUTER_BOUND('',#2068,.T.);
#1434=FACE_OUTER_BOUND('',#2069,.T.);
#1435=FACE_OUTER_BOUND('',#2070,.T.);
#1436=FACE_OUTER_BOUND('',#2071,.T.);
#1437=FACE_OUTER_BOUND('',#2073,.T.);
#2062=EDGE_LOOP('',(#6815,#6816,#6817,#6818,#6819,#6820,#6821,#6822,#6823));
#2063=EDGE_LOOP('',(#6824,#6825,#6826,#6827,#6828,#6829,#6830,#6831,#6832));
#2064=EDGE_LOOP('',(#6833,#6834,#6835,#6836));
#2065=EDGE_LOOP('',(#6837,#6838,#6839,#6840));
#2066=EDGE_LOOP('',(#6841,#6842,#6843,#6844));
#2067=EDGE_LOOP('',(#6845,#6846,#6847,#6848));
#2068=EDGE_LOOP('',(#6849,#6850,#6851,#6852));
#2069=EDGE_LOOP('',(#6853,#6854,#6855,#6856));
#2070=EDGE_LOOP('',(#6857,#6858,#6859,#6860));
#2071=EDGE_LOOP('',(#6861));
#2072=EDGE_LOOP('',(#6862));
#2073=EDGE_LOOP('',(#6863));
#2074=EDGE_LOOP('',(#6864));
#2782=CIRCLE('',#10516,0.38);
#2783=CIRCLE('',#10518,0.38);
#2784=CIRCLE('',#10523,0.2117);
#2785=CIRCLE('',#10524,0.2117);
#3296=LINE('',#15267,#3900);
#3297=LINE('',#15288,#3901);
#3298=LINE('',#15313,#3902);
#3299=LINE('',#15314,#3903);
#3300=LINE('',#15316,#3904);
#3301=LINE('',#15318,#3905);
#3302=LINE('',#15323,#3906);
#3303=LINE('',#15326,#3907);
#3304=LINE('',#15328,#3908);
#3900=VECTOR('',#12190,0.47094010767585);
#3901=VECTOR('',#12197,0.47094010767585);
#3902=VECTOR('',#12200,1.);
#3903=VECTOR('',#12201,1.);
#3904=VECTOR('',#12204,1.);
#3905=VECTOR('',#12207,1.);
#3906=VECTOR('',#12212,0.25);
#3907=VECTOR('',#12217,1.);
#3908=VECTOR('',#12220,1.);
#4533=VERTEX_POINT('',#15257);
#4534=VERTEX_POINT('',#15258);
#4535=VERTEX_POINT('',#15262);
#4536=VERTEX_POINT('',#15266);
#4537=VERTEX_POINT('',#15269);
#4538=VERTEX_POINT('',#15273);
#4539=VERTEX_POINT('',#15277);
#4540=VERTEX_POINT('',#15285);
#4541=VERTEX_POINT('',#15287);
#4542=VERTEX_POINT('',#15289);
#4543=VERTEX_POINT('',#15293);
#4544=VERTEX_POINT('',#15297);
#4545=VERTEX_POINT('',#15301);
#4546=VERTEX_POINT('',#15305);
#4547=VERTEX_POINT('',#15320);
#4548=VERTEX_POINT('',#15322);
#5394=EDGE_CURVE('',#4533,#4534,#510,.T.);
#5395=EDGE_CURVE('',#4535,#4533,#511,.T.);
#5396=EDGE_CURVE('',#4535,#4536,#3296,.T.);
#5397=EDGE_CURVE('',#4536,#4536,#2782,.T.);
#5398=EDGE_CURVE('',#4537,#4535,#512,.T.);
#5399=EDGE_CURVE('',#4538,#4537,#513,.T.);
#5400=EDGE_CURVE('',#4539,#4538,#514,.T.);
#5401=EDGE_CURVE('',#4534,#4539,#515,.T.);
#5402=EDGE_CURVE('',#4540,#4540,#2783,.T.);
#5403=EDGE_CURVE('',#4540,#4541,#3297,.T.);
#5404=EDGE_CURVE('',#4542,#4541,#516,.T.);
#5405=EDGE_CURVE('',#4543,#4542,#517,.T.);
#5406=EDGE_CURVE('',#4544,#4543,#518,.T.);
#5407=EDGE_CURVE('',#4545,#4544,#519,.T.);
#5408=EDGE_CURVE('',#4546,#4545,#520,.T.);
#5409=EDGE_CURVE('',#4541,#4546,#521,.T.);
#5410=EDGE_CURVE('',#4537,#4546,#3298,.T.);
#5411=EDGE_CURVE('',#4538,#4545,#3299,.T.);
#5412=EDGE_CURVE('',#4535,#4541,#3300,.T.);
#5413=EDGE_CURVE('',#4533,#4542,#3301,.T.);
#5414=EDGE_CURVE('',#4547,#4547,#2784,.F.);
#5415=EDGE_CURVE('',#4547,#4548,#3302,.T.);
#5416=EDGE_CURVE('',#4548,#4548,#2785,.F.);
#5417=EDGE_CURVE('',#4534,#4543,#3303,.T.);
#5418=EDGE_CURVE('',#4539,#4544,#3304,.T.);
#6815=ORIENTED_EDGE('',*,*,#5394,.F.);
#6816=ORIENTED_EDGE('',*,*,#5395,.F.);
#6817=ORIENTED_EDGE('',*,*,#5396,.T.);
#6818=ORIENTED_EDGE('',*,*,#5397,.F.);
#6819=ORIENTED_EDGE('',*,*,#5396,.F.);
#6820=ORIENTED_EDGE('',*,*,#5398,.F.);
#6821=ORIENTED_EDGE('',*,*,#5399,.F.);
#6822=ORIENTED_EDGE('',*,*,#5400,.F.);
#6823=ORIENTED_EDGE('',*,*,#5401,.F.);
#6824=ORIENTED_EDGE('',*,*,#5402,.F.);
#6825=ORIENTED_EDGE('',*,*,#5403,.T.);
#6826=ORIENTED_EDGE('',*,*,#5404,.F.);
#6827=ORIENTED_EDGE('',*,*,#5405,.F.);
#6828=ORIENTED_EDGE('',*,*,#5406,.F.);
#6829=ORIENTED_EDGE('',*,*,#5407,.F.);
#6830=ORIENTED_EDGE('',*,*,#5408,.F.);
#6831=ORIENTED_EDGE('',*,*,#5409,.F.);
#6832=ORIENTED_EDGE('',*,*,#5403,.F.);
#6833=ORIENTED_EDGE('',*,*,#5399,.T.);
#6834=ORIENTED_EDGE('',*,*,#5410,.T.);
#6835=ORIENTED_EDGE('',*,*,#5408,.T.);
#6836=ORIENTED_EDGE('',*,*,#5411,.F.);
#6837=ORIENTED_EDGE('',*,*,#5398,.T.);
#6838=ORIENTED_EDGE('',*,*,#5412,.T.);
#6839=ORIENTED_EDGE('',*,*,#5409,.T.);
#6840=ORIENTED_EDGE('',*,*,#5410,.F.);
#6841=ORIENTED_EDGE('',*,*,#5395,.T.);
#6842=ORIENTED_EDGE('',*,*,#5413,.T.);
#6843=ORIENTED_EDGE('',*,*,#5404,.T.);
#6844=ORIENTED_EDGE('',*,*,#5412,.F.);
#6845=ORIENTED_EDGE('',*,*,#5414,.F.);
#6846=ORIENTED_EDGE('',*,*,#5415,.T.);
#6847=ORIENTED_EDGE('',*,*,#5416,.T.);
#6848=ORIENTED_EDGE('',*,*,#5415,.F.);
#6849=ORIENTED_EDGE('',*,*,#5394,.T.);
#6850=ORIENTED_EDGE('',*,*,#5417,.T.);
#6851=ORIENTED_EDGE('',*,*,#5405,.T.);
#6852=ORIENTED_EDGE('',*,*,#5413,.F.);
#6853=ORIENTED_EDGE('',*,*,#5400,.T.);
#6854=ORIENTED_EDGE('',*,*,#5411,.T.);
#6855=ORIENTED_EDGE('',*,*,#5407,.T.);
#6856=ORIENTED_EDGE('',*,*,#5418,.F.);
#6857=ORIENTED_EDGE('',*,*,#5401,.T.);
#6858=ORIENTED_EDGE('',*,*,#5418,.T.);
#6859=ORIENTED_EDGE('',*,*,#5406,.T.);
#6860=ORIENTED_EDGE('',*,*,#5417,.F.);
#6861=ORIENTED_EDGE('',*,*,#5402,.T.);
#6862=ORIENTED_EDGE('',*,*,#5414,.T.);
#6863=ORIENTED_EDGE('',*,*,#5397,.T.);
#6864=ORIENTED_EDGE('',*,*,#5416,.F.);
#8647=PLANE('',#10519);
#8648=PLANE('',#10520);
#8649=PLANE('',#10521);
#8650=PLANE('',#10525);
#8651=PLANE('',#10526);
#8652=PLANE('',#10527);
#8653=PLANE('',#10528);
#8654=PLANE('',#10529);
#9032=ADVANCED_FACE('',(#1427),#532,.T.);
#9033=ADVANCED_FACE('',(#1428),#533,.T.);
#9034=ADVANCED_FACE('',(#1429),#8647,.T.);
#9035=ADVANCED_FACE('',(#1430),#8648,.T.);
#9036=ADVANCED_FACE('',(#1431),#8649,.T.);
#9037=ADVANCED_FACE('',(#1432),#1146,.F.);
#9038=ADVANCED_FACE('',(#1433),#8650,.T.);
#9039=ADVANCED_FACE('',(#1434),#8651,.T.);
#9040=ADVANCED_FACE('',(#1435),#8652,.T.);
#9041=ADVANCED_FACE('',(#1436,#887),#8653,.T.);
#9042=ADVANCED_FACE('',(#1437,#888),#8654,.F.);
#9488=CLOSED_SHELL('',(#9032,#9033,#9034,#9035,#9036,#9037,#9038,#9039,
#9040,#9041,#9042));
#10514=AXIS2_PLACEMENT_3D('',#15255,#12186,#12187);
#10515=AXIS2_PLACEMENT_3D('',#15256,#12188,#12189);
#10516=AXIS2_PLACEMENT_3D('',#15268,#12191,#12192);
#10517=AXIS2_PLACEMENT_3D('',#15284,#12193,#12194);
#10518=AXIS2_PLACEMENT_3D('',#15286,#12195,#12196);
#10519=AXIS2_PLACEMENT_3D('',#15312,#12198,#12199);
#10520=AXIS2_PLACEMENT_3D('',#15315,#12202,#12203);
#10521=AXIS2_PLACEMENT_3D('',#15317,#12205,#12206);
#10522=AXIS2_PLACEMENT_3D('',#15319,#12208,#12209);
#10523=AXIS2_PLACEMENT_3D('',#15321,#12210,#12211);
#10524=AXIS2_PLACEMENT_3D('',#15324,#12213,#12214);
#10525=AXIS2_PLACEMENT_3D('',#15325,#12215,#12216);
#10526=AXIS2_PLACEMENT_3D('',#15327,#12218,#12219);
#10527=AXIS2_PLACEMENT_3D('',#15329,#12221,#12222);
#10528=AXIS2_PLACEMENT_3D('',#15330,#12223,#12224);
#10529=AXIS2_PLACEMENT_3D('',#15331,#12225,#12226);
#12186=DIRECTION('axis',(0.,0.,1.));
#12187=DIRECTION('refdir',(1.,0.,0.));
#12188=DIRECTION('center_axis',(0.,1.,0.));
#12189=DIRECTION('ref_axis',(1.,0.,0.));
#12190=DIRECTION('',(0.866025403784439,-0.5,1.06057523872491E-16));
#12191=DIRECTION('center_axis',(0.,-1.,0.));
#12192=DIRECTION('ref_axis',(1.,0.,0.));
#12193=DIRECTION('center_axis',(0.,-1.,0.));
#12194=DIRECTION('ref_axis',(1.,0.,0.));
#12195=DIRECTION('center_axis',(0.,1.,0.));
#12196=DIRECTION('ref_axis',(1.,0.,0.));
#12197=DIRECTION('',(-0.866025403784439,-0.5,-1.06057523872491E-16));
#12198=DIRECTION('center_axis',(1.20185167898973E-16,0.,-1.));
#12199=DIRECTION('ref_axis',(-1.,0.,-1.20185167898973E-16));
#12200=DIRECTION('',(0.,1.,0.));
#12201=DIRECTION('',(0.,1.,0.));
#12202=DIRECTION('center_axis',(-0.866025403784439,0.,-0.5));
#12203=DIRECTION('ref_axis',(-0.5,0.,0.866025403784439));
#12204=DIRECTION('',(0.,1.,0.));
#12205=DIRECTION('center_axis',(-0.866025403784439,0.,0.5));
#12206=DIRECTION('ref_axis',(0.5,0.,0.866025403784439));
#12207=DIRECTION('',(0.,1.,0.));
#12208=DIRECTION('center_axis',(0.,1.,0.));
#12209=DIRECTION('ref_axis',(1.,0.,0.));
#12210=DIRECTION('center_axis',(0.,1.,0.));
#12211=DIRECTION('ref_axis',(1.,0.,0.));
#12212=DIRECTION('',(0.,-1.,0.));
#12213=DIRECTION('center_axis',(0.,1.,0.));
#12214=DIRECTION('ref_axis',(1.,0.,0.));
#12215=DIRECTION('center_axis',(-2.40370335797945E-16,0.,1.));
#12216=DIRECTION('ref_axis',(1.,0.,2.40370335797945E-16));
#12217=DIRECTION('',(0.,1.,0.));
#12218=DIRECTION('center_axis',(0.866025403784439,0.,-0.5));
#12219=DIRECTION('ref_axis',(-0.5,0.,-0.866025403784439));
#12220=DIRECTION('',(0.,1.,0.));
#12221=DIRECTION('center_axis',(0.866025403784439,0.,0.5));
#12222=DIRECTION('ref_axis',(0.5,0.,-0.866025403784439));
#12223=DIRECTION('center_axis',(0.,1.,0.));
#12224=DIRECTION('ref_axis',(1.,0.,0.));
#12225=DIRECTION('center_axis',(0.,1.,0.));
#12226=DIRECTION('ref_axis',(1.,0.,0.));
#15255=CARTESIAN_POINT('',(0.,0.,0.));
#15256=CARTESIAN_POINT('Origin',(0.,0.0525042956467857,0.));
#15257=CARTESIAN_POINT('',(-0.230940107675851,0.0472735643746089,0.4));
#15258=CARTESIAN_POINT('',(0.23094010767585,0.0472735643746089,0.4));
#15259=CARTESIAN_POINT('Ctrl Pts',(-0.230940107675851,0.0472735643746089,
0.4));
#15260=CARTESIAN_POINT('Ctrl Pts',(1.11022302462516E-16,-0.0193931022920578,
0.4));
#15261=CARTESIAN_POINT('Ctrl Pts',(0.23094010767585,0.0472735643746089,
0.4));
#15262=CARTESIAN_POINT('',(-0.461880215351701,0.0472735643746089,-5.6564012731995E-17));
#15263=CARTESIAN_POINT('Ctrl Pts',(-0.461880215351701,0.0472735643746089,
-5.6564012731995E-17));
#15264=CARTESIAN_POINT('Ctrl Pts',(-0.346410161513776,-0.0193931022920579,
0.2));
#15265=CARTESIAN_POINT('Ctrl Pts',(-0.230940107675851,0.0472735643746089,
0.4));
#15266=CARTESIAN_POINT('',(-0.38,-2.08166817117217E-17,-4.65365783675994E-17));
#15267=CARTESIAN_POINT('',(-0.47094010767585,0.0525042956467857,-5.7673529545534E-17));
#15268=CARTESIAN_POINT('Origin',(0.,0.,0.));
#15269=CARTESIAN_POINT('',(-0.23094010767585,0.0472735643746089,-0.4));
#15270=CARTESIAN_POINT('Ctrl Pts',(-0.23094010767585,0.0472735643746089,
-0.4));
#15271=CARTESIAN_POINT('Ctrl Pts',(-0.346410161513775,-0.0193931022920578,
-0.2));
#15272=CARTESIAN_POINT('Ctrl Pts',(-0.461880215351701,0.0472735643746089,
-5.6564012731995E-17));
#15273=CARTESIAN_POINT('',(0.23094010767585,0.0472735643746089,-0.4));
#15274=CARTESIAN_POINT('Ctrl Pts',(0.23094010767585,0.0472735643746089,
-0.4));
#15275=CARTESIAN_POINT('Ctrl Pts',(0.,-0.0193931022920578,-0.4));
#15276=CARTESIAN_POINT('Ctrl Pts',(-0.23094010767585,0.0472735643746089,
-0.4));
#15277=CARTESIAN_POINT('',(0.461880215351701,0.0472735643746089,0.));
#15278=CARTESIAN_POINT('Ctrl Pts',(0.461880215351701,0.0472735643746089,
0.));
#15279=CARTESIAN_POINT('Ctrl Pts',(0.346410161513776,-0.019393102292058,
-0.2));
#15280=CARTESIAN_POINT('Ctrl Pts',(0.23094010767585,0.0472735643746089,
-0.4));
#15281=CARTESIAN_POINT('Ctrl Pts',(0.23094010767585,0.0472735643746089,
0.4));
#15282=CARTESIAN_POINT('Ctrl Pts',(0.346410161513776,-0.0193931022920577,
0.2));
#15283=CARTESIAN_POINT('Ctrl Pts',(0.461880215351701,0.0472735643746089,
0.));
#15284=CARTESIAN_POINT('Origin',(0.,0.417495704353214,0.));
#15285=CARTESIAN_POINT('',(-0.38,0.47,-4.65365783675994E-17));
#15286=CARTESIAN_POINT('Origin',(0.,0.47,0.));
#15287=CARTESIAN_POINT('',(-0.461880215351701,0.422726435625391,-5.6564012731995E-17));
#15288=CARTESIAN_POINT('',(-0.47094010767585,0.417495704353214,-5.7673529545534E-17));
#15289=CARTESIAN_POINT('',(-0.230940107675851,0.422726435625391,0.4));
#15290=CARTESIAN_POINT('Ctrl Pts',(-0.230940107675851,0.422726435625391,
0.4));
#15291=CARTESIAN_POINT('Ctrl Pts',(-0.346410161513776,0.489393102292058,
0.2));
#15292=CARTESIAN_POINT('Ctrl Pts',(-0.461880215351701,0.422726435625391,
-5.6564012731995E-17));
#15293=CARTESIAN_POINT('',(0.23094010767585,0.422726435625391,0.4));
#15294=CARTESIAN_POINT('Ctrl Pts',(0.23094010767585,0.422726435625391,0.4));
#15295=CARTESIAN_POINT('Ctrl Pts',(8.32667268468867E-17,0.489393102292058,
0.4));
#15296=CARTESIAN_POINT('Ctrl Pts',(-0.230940107675851,0.422726435625391,
0.4));
#15297=CARTESIAN_POINT('',(0.461880215351701,0.422726435625391,0.));
#15298=CARTESIAN_POINT('Ctrl Pts',(0.461880215351701,0.422726435625391,
0.));
#15299=CARTESIAN_POINT('Ctrl Pts',(0.346410161513776,0.489393102292058,
0.2));
#15300=CARTESIAN_POINT('Ctrl Pts',(0.23094010767585,0.422726435625391,0.4));
#15301=CARTESIAN_POINT('',(0.23094010767585,0.422726435625391,-0.4));
#15302=CARTESIAN_POINT('Ctrl Pts',(0.23094010767585,0.422726435625391,-0.4));
#15303=CARTESIAN_POINT('Ctrl Pts',(0.346410161513775,0.489393102292058,
-0.2));
#15304=CARTESIAN_POINT('Ctrl Pts',(0.461880215351701,0.422726435625391,
0.));
#15305=CARTESIAN_POINT('',(-0.23094010767585,0.422726435625391,-0.4));
#15306=CARTESIAN_POINT('Ctrl Pts',(-0.23094010767585,0.422726435625391,
-0.4));
#15307=CARTESIAN_POINT('Ctrl Pts',(-5.55111512312578E-17,0.489393102292058,
-0.4));
#15308=CARTESIAN_POINT('Ctrl Pts',(0.23094010767585,0.422726435625391,-0.4));
#15309=CARTESIAN_POINT('Ctrl Pts',(-0.461880215351701,0.422726435625391,
-5.6564012731995E-17));
#15310=CARTESIAN_POINT('Ctrl Pts',(-0.346410161513776,0.489393102292058,
-0.2));
#15311=CARTESIAN_POINT('Ctrl Pts',(-0.23094010767585,0.422726435625391,
-0.4));
#15312=CARTESIAN_POINT('Origin',(0.23094010767585,0.,-0.4));
#15313=CARTESIAN_POINT('',(-0.23094010767585,0.,-0.4));
#15314=CARTESIAN_POINT('',(0.23094010767585,0.,-0.4));
#15315=CARTESIAN_POINT('Origin',(-0.23094010767585,0.,-0.4));
#15316=CARTESIAN_POINT('',(-0.461880215351701,0.,-5.6564012731995E-17));
#15317=CARTESIAN_POINT('Origin',(-0.461880215351701,0.,-5.6564012731995E-17));
#15318=CARTESIAN_POINT('',(-0.230940107675851,0.,0.4));
#15319=CARTESIAN_POINT('Origin',(0.,0.,0.));
#15320=CARTESIAN_POINT('',(-0.2117,0.47,2.59257727379495E-17));
#15321=CARTESIAN_POINT('Origin',(0.,0.47,0.));
#15322=CARTESIAN_POINT('',(-0.2117,0.,2.59257727379495E-17));
#15323=CARTESIAN_POINT('',(-0.2117,0.,2.59257727379495E-17));
#15324=CARTESIAN_POINT('Origin',(0.,0.,0.));
#15325=CARTESIAN_POINT('Origin',(-0.230940107675851,0.,0.4));
#15326=CARTESIAN_POINT('',(0.23094010767585,0.,0.4));
#15327=CARTESIAN_POINT('Origin',(0.461880215351701,0.,0.));
#15328=CARTESIAN_POINT('',(0.461880215351701,0.,0.));
#15329=CARTESIAN_POINT('Origin',(0.23094010767585,0.,0.4));
#15330=CARTESIAN_POINT('Origin',(0.,0.47,0.));
#15331=CARTESIAN_POINT('Origin',(0.,0.,0.));
#18919=UNCERTAINTY_MEASURE_WITH_UNIT(LENGTH_MEASURE(0.001),#19044,
'DISTANCE_ACCURACY_VALUE',
'Maximum model space distance between geometric entities at asserted c
onnectivities');
#18972=UNCERTAINTY_MEASURE_WITH_UNIT(LENGTH_MEASURE(0.001),#19044,
'DISTANCE_ACCURACY_VALUE',
'Maximum model space distance between geometric entities at asserted c
onnectivities');
#18990=(
GEOMETRIC_REPRESENTATION_CONTEXT(3)
GLOBAL_UNCERTAINTY_ASSIGNED_CONTEXT((#18919))
GLOBAL_UNIT_ASSIGNED_CONTEXT((#19044,#19046,#19047))
REPRESENTATION_CONTEXT('','3D')
);
#19043=(
GEOMETRIC_REPRESENTATION_CONTEXT(3)
GLOBAL_UNCERTAINTY_ASSIGNED_CONTEXT((#18972))
GLOBAL_UNIT_ASSIGNED_CONTEXT((#19044,#19046,#19047))
REPRESENTATION_CONTEXT('','3D')
);
#19044=(
LENGTH_UNIT()
NAMED_UNIT(*)
SI_UNIT(.CENTI.,.METRE.)
);
#19046=(
NAMED_UNIT(*)
PLANE_ANGLE_UNIT()
SI_UNIT($,.RADIAN.)
);
#19047=(
NAMED_UNIT(*)
SI_UNIT($,.STERADIAN.)
SOLID_ANGLE_UNIT()
);
#19065=SHAPE_DEFINITION_REPRESENTATION(#19135,#19323);
#19135=PRODUCT_DEFINITION_SHAPE('',$,#19394);
#19323=SHAPE_REPRESENTATION('',(#10514),#18990);
#19376=PRODUCT_DEFINITION_CONTEXT('part definition',#19588,'design');
#19394=PRODUCT_DEFINITION('2026-11-03-00-38-46-457','Hex Nut - M5',#19464,
#19376);
#19464=PRODUCT_DEFINITION_FORMATION('',$,#19607);
#19588=APPLICATION_CONTEXT(
'Core Data for Automotive Mechanical Design Process');
#19589=PRODUCT_CONTEXT('part definition',#19588,'mechanical');
#19607=PRODUCT('2026-11-03-00-38-46-457','Hex Nut - M5','Hex Nut - M5',
(#19589));
#19663=PRESENTATION_STYLE_ASSIGNMENT((#19669));
#19669=SURFACE_STYLE_USAGE(.BOTH.,#19675);
#19675=SURFACE_SIDE_STYLE('',(#19681));
#19681=SURFACE_STYLE_FILL_AREA(#19687);
#19687=FILL_AREA_STYLE('CAD Library Painted - Graphite',(#19693));
#19693=FILL_AREA_STYLE_COLOUR('CAD Library Painted - Graphite',#19699);
#19699=COLOUR_RGB('CAD Library Painted - Graphite',0.168627450980392,0.192156862745098,
0.231372549019608);
ENDSEC;
END-ISO-10303-21;
